ISO-10303-21;
HEADER;
/* Generated by software containing ST-Developer
 * from STEP Tools, Inc. (www.steptools.com) 
 */

FILE_DESCRIPTION(
/* description */ ('Torque wrench calibration arm'),
/* implementation_level */ '2;1');

FILE_NAME(
/* name */ 'Outer ring (1).step',
/* time_stamp */ '2026-10-28T03:24:52-07:00',
/* author */ (''),
/* organization */ (''),
/* preprocessor_version */ 'ST-DEVELOPER v20.2',
/* originating_system */ 'Autodesk Translation Framework v15.17.0.0',
/* authorisation */ '');

FILE_SCHEMA (('AUTOMOTIVE_DESIGN { 1 0 10303 214 3 1 1 }'));
ENDSEC;

DATA;
#10=MECHANICAL_DESIGN_GEOMETRIC_PRESENTATION_REPRESENTATION('',(#459),#12783);
#343=CONICAL_SURFACE('',#7570,1.47,0.785398163397449);
#344=CONICAL_SURFACE('',#7574,1.47,0.785398163397449);
#351=TOROIDAL_SURFACE('',#7559,1.,0.247676);
#376=SHAPE_REPRESENTATION_RELATIONSHIP('SRR','None',#12960,#413);
#413=ADVANCED_BREP_SHAPE_REPRESENTATION('',(#511),#12769);
#459=STYLED_ITEM('',(#13212),#511);
#511=MANIFOLD_SOLID_BREP('Body1',#6530);
#624=FACE_BOUND('',#1658,.T.);
#625=FACE_BOUND('',#1663,.T.);
#823=PLANE('',#7567);
#824=PLANE('',#7576);
#1167=FACE_OUTER_BOUND('',#1655,.T.);
#1168=FACE_OUTER_BOUND('',#1656,.T.);
#1169=FACE_OUTER_BOUND('',#1657,.T.);
#1170=FACE_OUTER_BOUND('',#1659,.T.);
#1171=FACE_OUTER_BOUND('',#1660,.T.);
#1172=FACE_OUTER_BOUND('',#1661,.T.);
#1173=FACE_OUTER_BOUND('',#1662,.T.);
#1174=FACE_OUTER_BOUND('',#1664,.T.);
#1655=EDGE_LOOP('',(#5591,#5592,#5593,#5594,#5595,#5596));
#1656=EDGE_LOOP('',(#5597,#5598,#5599,#5600,#5601));
#1657=EDGE_LOOP('',(#5602));
#1658=EDGE_LOOP('',(#5603));
#1659=EDGE_LOOP('',(#5604,#5605,#5606,#5607));
#1660=EDGE_LOOP('',(#5608,#5609,#5610,#5611));
#1661=EDGE_LOOP('',(#5612,#5613,#5614,#5615));
#1662=EDGE_LOOP('',(#5616));
#1663=EDGE_LOOP('',(#5617));
#1664=EDGE_LOOP('',(#5618,#5619,#5620,#5621,#5622));
#2125=LINE('',#11885,#2540);
#2126=LINE('',#11894,#2541);
#2127=LINE('',#11898,#2542);
#2128=LINE('',#11902,#2543);
#2129=LINE('',#11905,#2544);
#2540=VECTOR('',#9363,1.023815);
#2541=VECTOR('',#9374,1.47);
#2542=VECTOR('',#9379,1.5);
#2543=VECTOR('',#9384,1.47);
#2544=VECTOR('',#9389,1.023815);
#2867=CIRCLE('',#7560,1.023815);
#2868=CIRCLE('',#7561,1.023815);
#2869=CIRCLE('',#7562,0.247676);
#2870=CIRCLE('',#7563,1.023815);
#2871=CIRCLE('',#7564,1.023815);
#2872=CIRCLE('',#7566,1.023815);
#2873=CIRCLE('',#7568,1.44);
#2874=CIRCLE('',#7569,1.023815);
#2875=CIRCLE('',#7571,1.5);
#2876=CIRCLE('',#7573,1.5);
#2877=CIRCLE('',#7575,1.44);
#3392=VERTEX_POINT('',#11873);
#3393=VERTEX_POINT('',#11874);
#3394=VERTEX_POINT('',#11877);
#3395=VERTEX_POINT('',#11879);
#3396=VERTEX_POINT('',#11883);
#3397=VERTEX_POINT('',#11887);
#3398=VERTEX_POINT('',#11889);
#3399=VERTEX_POINT('',#11892);
#3400=VERTEX_POINT('',#11896);
#3401=VERTEX_POINT('',#11900);
#4153=EDGE_CURVE('',#3392,#3393,#2867,.T.);
#4154=EDGE_CURVE('',#3393,#3392,#2868,.T.);
#4155=EDGE_CURVE('',#3393,#3394,#2869,.T.);
#4156=EDGE_CURVE('',#3395,#3394,#2870,.T.);
#4157=EDGE_CURVE('',#3394,#3395,#2871,.T.);
#4158=EDGE_CURVE('',#3396,#3396,#2872,.T.);
#4159=EDGE_CURVE('',#3396,#3395,#2125,.T.);
#4160=EDGE_CURVE('',#3397,#3397,#2873,.T.);
#4161=EDGE_CURVE('',#3398,#3398,#2874,.T.);
#4162=EDGE_CURVE('',#3399,#3399,#2875,.T.);
#4163=EDGE_CURVE('',#3399,#3397,#2126,.T.);
#4164=EDGE_CURVE('',#3400,#3400,#2876,.T.);
#4165=EDGE_CURVE('',#3400,#3399,#2127,.T.);
#4166=EDGE_CURVE('',#3401,#3401,#2877,.T.);
#4167=EDGE_CURVE('',#3401,#3400,#2128,.T.);
#4168=EDGE_CURVE('',#3392,#3398,#2129,.T.);
#5591=ORIENTED_EDGE('',*,*,#4153,.F.);
#5592=ORIENTED_EDGE('',*,*,#4154,.F.);
#5593=ORIENTED_EDGE('',*,*,#4155,.T.);
#5594=ORIENTED_EDGE('',*,*,#4156,.F.);
#5595=ORIENTED_EDGE('',*,*,#4157,.F.);
#5596=ORIENTED_EDGE('',*,*,#4155,.F.);
#5597=ORIENTED_EDGE('',*,*,#4158,.T.);
#5598=ORIENTED_EDGE('',*,*,#4159,.T.);
#5599=ORIENTED_EDGE('',*,*,#4156,.T.);
#5600=ORIENTED_EDGE('',*,*,#4157,.T.);
#5601=ORIENTED_EDGE('',*,*,#4159,.F.);
#5602=ORIENTED_EDGE('',*,*,#4160,.F.);
#5603=ORIENTED_EDGE('',*,*,#4161,.T.);
#5604=ORIENTED_EDGE('',*,*,#4162,.F.);
#5605=ORIENTED_EDGE('',*,*,#4163,.T.);
#5606=ORIENTED_EDGE('',*,*,#4160,.T.);
#5607=ORIENTED_EDGE('',*,*,#4163,.F.);
#5608=ORIENTED_EDGE('',*,*,#4164,.F.);
#5609=ORIENTED_EDGE('',*,*,#4165,.T.);
#5610=ORIENTED_EDGE('',*,*,#4162,.T.);
#5611=ORIENTED_EDGE('',*,*,#4165,.F.);
#5612=ORIENTED_EDGE('',*,*,#4166,.F.);
#5613=ORIENTED_EDGE('',*,*,#4167,.T.);
#5614=ORIENTED_EDGE('',*,*,#4164,.T.);
#5615=ORIENTED_EDGE('',*,*,#4167,.F.);
#5616=ORIENTED_EDGE('',*,*,#4166,.T.);
#5617=ORIENTED_EDGE('',*,*,#4158,.F.);
#5618=ORIENTED_EDGE('',*,*,#4153,.T.);
#5619=ORIENTED_EDGE('',*,*,#4154,.T.);
#5620=ORIENTED_EDGE('',*,*,#4168,.T.);
#5621=ORIENTED_EDGE('',*,*,#4161,.F.);
#5622=ORIENTED_EDGE('',*,*,#4168,.F.);
#6071=CYLINDRICAL_SURFACE('',#7565,1.023815);
#6072=CYLINDRICAL_SURFACE('',#7572,1.5);
#6073=CYLINDRICAL_SURFACE('',#7577,1.023815);
#6392=ADVANCED_FACE('',(#1167),#351,.F.);
#6393=ADVANCED_FACE('',(#1168),#6071,.F.);
#6394=ADVANCED_FACE('',(#1169,#624),#823,.T.);
#6395=ADVANCED_FACE('',(#1170),#343,.T.);
#6396=ADVANCED_FACE('',(#1171),#6072,.T.);
#6397=ADVANCED_FACE('',(#1172),#344,.T.);
#6398=ADVANCED_FACE('',(#1173,#625),#824,.T.);
#6399=ADVANCED_FACE('',(#1174),#6073,.F.);
#6530=CLOSED_SHELL('',(#6392,#6393,#6394,#6395,#6396,#6397,#6398,#6399));
#7558=AXIS2_PLACEMENT_3D('',#11871,#9345,#9346);
#7559=AXIS2_PLACEMENT_3D('',#11872,#9347,#9348);
#7560=AXIS2_PLACEMENT_3D('',#11875,#9349,#9350);
#7561=AXIS2_PLACEMENT_3D('',#11876,#9351,#9352);
#7562=AXIS2_PLACEMENT_3D('',#11878,#9353,#9354);
#7563=AXIS2_PLACEMENT_3D('',#11880,#9355,#9356);
#7564=AXIS2_PLACEMENT_3D('',#11881,#9357,#9358);
#7565=AXIS2_PLACEMENT_3D('',#11882,#9359,#9360);
#7566=AXIS2_PLACEMENT_3D('',#11884,#9361,#9362);
#7567=AXIS2_PLACEMENT_3D('',#11886,#9364,#9365);
#7568=AXIS2_PLACEMENT_3D('',#11888,#9366,#9367);
#7569=AXIS2_PLACEMENT_3D('',#11890,#9368,#9369);
#7570=AXIS2_PLACEMENT_3D('',#11891,#9370,#9371);
#7571=AXIS2_PLACEMENT_3D('',#11893,#9372,#9373);
#7572=AXIS2_PLACEMENT_3D('',#11895,#9375,#9376);
#7573=AXIS2_PLACEMENT_3D('',#11897,#9377,#9378);
#7574=AXIS2_PLACEMENT_3D('',#11899,#9380,#9381);
#7575=AXIS2_PLACEMENT_3D('',#11901,#9382,#9383);
#7576=AXIS2_PLACEMENT_3D('',#11903,#9385,#9386);
#7577=AXIS2_PLACEMENT_3D('',#11904,#9387,#9388);
#9345=DIRECTION('axis',(0.,0.,1.));
#9346=DIRECTION('refdir',(1.,0.,0.));
#9347=DIRECTION('center_axis',(0.,-1.,0.));
#9348=DIRECTION('ref_axis',(0.,0.,-1.));
#9349=DIRECTION('center_axis',(0.,-1.,0.));
#9350=DIRECTION('ref_axis',(1.,0.,0.));
#9351=DIRECTION('center_axis',(0.,-1.,0.));
#9352=DIRECTION('ref_axis',(1.,0.,0.));
#9353=DIRECTION('center_axis',(1.,0.,1.22464679914735E-16));
#9354=DIRECTION('ref_axis',(-1.22464679914735E-16,0.,1.));
#9355=DIRECTION('center_axis',(0.,1.,0.));
#9356=DIRECTION('ref_axis',(1.,0.,0.));
#9357=DIRECTION('center_axis',(0.,1.,0.));
#9358=DIRECTION('ref_axis',(1.,0.,0.));
#9359=DIRECTION('center_axis',(0.,-1.,0.));
#9360=DIRECTION('ref_axis',(1.,0.,0.));
#9361=DIRECTION('center_axis',(0.,-1.,0.));
#9362=DIRECTION('ref_axis',(1.,0.,0.));
#9363=DIRECTION('',(0.,1.,0.));
#9364=DIRECTION('center_axis',(0.,1.,0.));
#9365=DIRECTION('ref_axis',(0.,0.,1.));
#9366=DIRECTION('center_axis',(0.,-1.,0.));
#9367=DIRECTION('ref_axis',(1.,0.,0.));
#9368=DIRECTION('center_axis',(0.,-1.,0.));
#9369=DIRECTION('ref_axis',(1.,0.,0.));
#9370=DIRECTION('center_axis',(0.,-1.,0.));
#9371=DIRECTION('ref_axis',(1.,0.,0.));
#9372=DIRECTION('center_axis',(0.,-1.,0.));
#9373=DIRECTION('ref_axis',(1.,0.,0.));
#9374=DIRECTION('',(0.707106781186548,0.707106781186547,8.65956056235494E-17));
#9375=DIRECTION('center_axis',(0.,-1.,0.));
#9376=DIRECTION('ref_axis',(1.,0.,0.));
#9377=DIRECTION('center_axis',(0.,-1.,0.));
#9378=DIRECTION('ref_axis',(1.,0.,0.));
#9379=DIRECTION('',(0.,1.,0.));
#9380=DIRECTION('center_axis',(0.,1.,0.));
#9381=DIRECTION('ref_axis',(1.,0.,0.));
#9382=DIRECTION('center_axis',(0.,-1.,0.));
#9383=DIRECTION('ref_axis',(1.,0.,0.));
#9384=DIRECTION('',(-0.707106781186548,0.707106781186547,-8.65956056235494E-17));
#9385=DIRECTION('center_axis',(0.,-1.,0.));
#9386=DIRECTION('ref_axis',(0.,0.,-1.));
#9387=DIRECTION('center_axis',(0.,-1.,0.));
#9388=DIRECTION('ref_axis',(1.,0.,0.));
#9389=DIRECTION('',(0.,1.,0.));
#11871=CARTESIAN_POINT('',(0.,0.,0.));
#11872=CARTESIAN_POINT('Origin',(0.,0.,0.));
#11873=CARTESIAN_POINT('',(-1.023815,0.246528389340863,-1.25381176266905E-16));
#11874=CARTESIAN_POINT('',(-1.25381176266905E-16,0.246528389340863,1.023815));
#11875=CARTESIAN_POINT('Origin',(0.,0.246528389340863,0.));
#11876=CARTESIAN_POINT('Origin',(0.,0.246528389340863,0.));
#11877=CARTESIAN_POINT('',(-1.25381176266905E-16,-0.246528389340863,1.023815));
#11878=CARTESIAN_POINT('Origin',(-1.22464679914735E-16,0.,1.));
#11879=CARTESIAN_POINT('',(-1.023815,-0.246528389340863,1.25381176266905E-16));
#11880=CARTESIAN_POINT('Origin',(0.,-0.246528389340863,0.));
#11881=CARTESIAN_POINT('Origin',(0.,-0.246528389340863,0.));
#11882=CARTESIAN_POINT('Origin',(0.,0.,0.));
#11883=CARTESIAN_POINT('',(-1.023815,-0.45,-1.25381176266905E-16));
#11884=CARTESIAN_POINT('Origin',(0.,-0.45,0.));
#11885=CARTESIAN_POINT('',(-1.023815,0.,-1.25381176266905E-16));
#11886=CARTESIAN_POINT('Origin',(1.44,0.45,0.));
#11887=CARTESIAN_POINT('',(-1.44,0.45,-1.76349139077219E-16));
#11888=CARTESIAN_POINT('Origin',(0.,0.45,0.));
#11889=CARTESIAN_POINT('',(-1.023815,0.45,-1.25381176266905E-16));
#11890=CARTESIAN_POINT('Origin',(0.,0.45,0.));
#11891=CARTESIAN_POINT('Origin',(0.,0.42,0.));
#11892=CARTESIAN_POINT('',(-1.5,0.39,-1.83697019872103E-16));
#11893=CARTESIAN_POINT('Origin',(0.,0.39,0.));
#11894=CARTESIAN_POINT('',(-1.47,0.42,-1.80023079474661E-16));
#11895=CARTESIAN_POINT('Origin',(0.,0.,0.));
#11896=CARTESIAN_POINT('',(-1.5,-0.39,-1.83697019872103E-16));
#11897=CARTESIAN_POINT('Origin',(0.,-0.39,0.));
#11898=CARTESIAN_POINT('',(-1.5,0.,-1.83697019872103E-16));
#11899=CARTESIAN_POINT('Origin',(0.,-0.42,0.));
#11900=CARTESIAN_POINT('',(-1.44,-0.45,-1.76349139077219E-16));
#11901=CARTESIAN_POINT('Origin',(0.,-0.45,0.));
#11902=CARTESIAN_POINT('',(-1.47,-0.42,-1.80023079474661E-16));
#11903=CARTESIAN_POINT('Origin',(1.023815,-0.45,0.));
#11904=CARTESIAN_POINT('Origin',(0.,0.,0.));
#11905=CARTESIAN_POINT('',(-1.023815,0.,-1.25381176266905E-16));
#12725=UNCERTAINTY_MEASURE_WITH_UNIT(LENGTH_MEASURE(0.001),#12784,
'DISTANCE_ACCURACY_VALUE',
'Maximum model space distance between geometric entities at asserted c
onnectivities');
#12739=UNCERTAINTY_MEASURE_WITH_UNIT(LENGTH_MEASURE(0.001),#12784,
'DISTANCE_ACCURACY_VALUE',
'Maximum model space distance between geometric entities at asserted c
onnectivities');
#12769=(
GEOMETRIC_REPRESENTATION_CONTEXT(3)
GLOBAL_UNCERTAINTY_ASSIGNED_CONTEXT((#12725))
GLOBAL_UNIT_ASSIGNED_CONTEXT((#12784,#12786,#12787))
REPRESENTATION_CONTEXT('','3D')
);
#12783=(
GEOMETRIC_REPRESENTATION_CONTEXT(3)
GLOBAL_UNCERTAINTY_ASSIGNED_CONTEXT((#12739))
GLOBAL_UNIT_ASSIGNED_CONTEXT((#12784,#12786,#12787))
REPRESENTATION_CONTEXT('','3D')
);
#12784=(
LENGTH_UNIT()
NAMED_UNIT(*)
SI_UNIT(.CENTI.,.METRE.)
);
#12786=(
NAMED_UNIT(*)
PLANE_ANGLE_UNIT()
SI_UNIT($,.RADIAN.)
);
#12787=(
NAMED_UNIT(*)
SI_UNIT($,.STERADIAN.)
SOLID_ANGLE_UNIT()
);
#12817=SHAPE_DEFINITION_REPRESENTATION(#12886,#12960);
#12886=PRODUCT_DEFINITION_SHAPE('',$,#13004);
#12960=SHAPE_REPRESENTATION('',(#7558),#12769);
#12974=PRODUCT_DEFINITION_CONTEXT('part definition',#13105,'design');
#13004=PRODUCT_DEFINITION('Outer ring (1)','Outer ring (1)',#13047,#12974);
#13047=PRODUCT_DEFINITION_FORMATION('',$,#13136);
#13105=APPLICATION_CONTEXT(
'Core Data for Automotive Mechanical Design Process');
#13106=PRODUCT_CONTEXT('part definition',#13105,'mechanical');
#13136=PRODUCT('Outer ring (1)','Outer ring (1)','Outer ring (1)',(#13106));
#13206=COLOUR_RGB('Grey',0.48,0.52,0.57);
#13207=FILL_AREA_STYLE_COLOUR('',#13206);
#13208=FILL_AREA_STYLE('',(#13207));
#13209=SURFACE_STYLE_FILL_AREA(#13208);
#13210=SURFACE_SIDE_STYLE('',(#13209));
#13211=SURFACE_STYLE_USAGE(.BOTH.,#13210);
#13212=PRESENTATION_STYLE_ASSIGNMENT((#13211));
ENDSEC;
END-ISO-10303-21;
